ISO-10303-21;
HEADER;
/* Generated by software containing ST-Developer
 * from STEP Tools, Inc. (www.steptools.com) 
 */

FILE_DESCRIPTION(
/* description */ ('Bearing friction torque test rig'),
/* implementation_level */ '2;1');

FILE_NAME(
/* name */ 'Support cap (1).step',
/* time_stamp */ '2026-10-28T03:24:04-07:00',
/* author */ (''),
/* organization */ (''),
/* preprocessor_version */ 'ST-DEVELOPER v20.2',
/* originating_system */ 'Autodesk Translation Framework v15.17.0.0',
/* authorisation */ '');

FILE_SCHEMA (('AUTOMOTIVE_DESIGN { 1 0 10303 214 3 1 1 }'));
ENDSEC;

DATA;
#10=MECHANICAL_DESIGN_GEOMETRIC_PRESENTATION_REPRESENTATION('',(#542),#14822);
#464=SHAPE_REPRESENTATION_RELATIONSHIP('SRR','None',#15003,#503);
#503=ADVANCED_BREP_SHAPE_REPRESENTATION('',(#596),#14783);
#542=STYLED_ITEM('',(#15277),#596);
#596=MANIFOLD_SOLID_BREP('Body1',#7658);
#695=FACE_BOUND('',#1650,.T.);
#696=FACE_BOUND('',#1654,.T.);
#697=FACE_BOUND('',#1655,.T.);
#698=FACE_BOUND('',#1656,.T.);
#699=FACE_BOUND('',#1657,.T.);
#700=FACE_BOUND('',#1658,.T.);
#701=FACE_BOUND('',#1660,.T.);
#702=FACE_BOUND('',#1661,.T.);
#703=FACE_BOUND('',#1662,.T.);
#704=FACE_BOUND('',#1663,.T.);
#705=FACE_BOUND('',#1664,.T.);
#894=PLANE('',#8274);
#895=PLANE('',#8281);
#896=PLANE('',#8282);
#1148=FACE_OUTER_BOUND('',#1644,.T.);
#1149=FACE_OUTER_BOUND('',#1645,.T.);
#1150=FACE_OUTER_BOUND('',#1646,.T.);
#1151=FACE_OUTER_BOUND('',#1647,.T.);
#1152=FACE_OUTER_BOUND('',#1648,.T.);
#1153=FACE_OUTER_BOUND('',#1649,.T.);
#1154=FACE_OUTER_BOUND('',#1651,.T.);
#1155=FACE_OUTER_BOUND('',#1652,.T.);
#1156=FACE_OUTER_BOUND('',#1653,.T.);
#1157=FACE_OUTER_BOUND('',#1659,.T.);
#1644=EDGE_LOOP('',(#5388,#5389,#5390,#5391));
#1645=EDGE_LOOP('',(#5392,#5393,#5394,#5395));
#1646=EDGE_LOOP('',(#5396,#5397,#5398,#5399));
#1647=EDGE_LOOP('',(#5400,#5401,#5402,#5403));
#1648=EDGE_LOOP('',(#5404,#5405,#5406,#5407));
#1649=EDGE_LOOP('',(#5408));
#1650=EDGE_LOOP('',(#5409));
#1651=EDGE_LOOP('',(#5410,#5411,#5412,#5413));
#1652=EDGE_LOOP('',(#5414,#5415,#5416,#5417));
#1653=EDGE_LOOP('',(#5418));
#1654=EDGE_LOOP('',(#5419));
#1655=EDGE_LOOP('',(#5420));
#1656=EDGE_LOOP('',(#5421));
#1657=EDGE_LOOP('',(#5422));
#1658=EDGE_LOOP('',(#5423));
#1659=EDGE_LOOP('',(#5424));
#1660=EDGE_LOOP('',(#5425));
#1661=EDGE_LOOP('',(#5426));
#1662=EDGE_LOOP('',(#5427));
#1663=EDGE_LOOP('',(#5428));
#1664=EDGE_LOOP('',(#5429));
#2277=LINE('',#11917,#2721);
#2278=LINE('',#11923,#2722);
#2279=LINE('',#11929,#2723);
#2280=LINE('',#11935,#2724);
#2281=LINE('',#11941,#2725);
#2282=LINE('',#11949,#2726);
#2283=LINE('',#11954,#2727);
#2721=VECTOR('',#9462,0.225);
#2722=VECTOR('',#9469,0.225);
#2723=VECTOR('',#9476,0.225);
#2724=VECTOR('',#9483,0.225);
#2725=VECTOR('',#9490,1.59);
#2726=VECTOR('',#9501,1.1);
#2727=VECTOR('',#9506,2.5);
#3166=CIRCLE('',#8260,0.225);
#3167=CIRCLE('',#8261,0.225);
#3168=CIRCLE('',#8263,0.225);
#3169=CIRCLE('',#8264,0.225);
#3170=CIRCLE('',#8266,0.225);
#3171=CIRCLE('',#8267,0.225);
#3172=CIRCLE('',#8269,0.225);
#3173=CIRCLE('',#8270,0.225);
#3174=CIRCLE('',#8272,1.59);
#3175=CIRCLE('',#8273,1.59);
#3176=CIRCLE('',#8275,1.1);
#3177=CIRCLE('',#8277,1.1);
#3178=CIRCLE('',#8279,2.5);
#3179=CIRCLE('',#8280,2.5);
#3633=VERTEX_POINT('',#11914);
#3634=VERTEX_POINT('',#11916);
#3635=VERTEX_POINT('',#11920);
#3636=VERTEX_POINT('',#11922);
#3637=VERTEX_POINT('',#11926);
#3638=VERTEX_POINT('',#11928);
#3639=VERTEX_POINT('',#11932);
#3640=VERTEX_POINT('',#11934);
#3641=VERTEX_POINT('',#11938);
#3642=VERTEX_POINT('',#11940);
#3643=VERTEX_POINT('',#11944);
#3644=VERTEX_POINT('',#11947);
#3645=VERTEX_POINT('',#11951);
#3646=VERTEX_POINT('',#11953);
#4320=EDGE_CURVE('',#3633,#3633,#3166,.T.);
#4321=EDGE_CURVE('',#3633,#3634,#2277,.T.);
#4322=EDGE_CURVE('',#3634,#3634,#3167,.T.);
#4323=EDGE_CURVE('',#3635,#3635,#3168,.T.);
#4324=EDGE_CURVE('',#3635,#3636,#2278,.T.);
#4325=EDGE_CURVE('',#3636,#3636,#3169,.T.);
#4326=EDGE_CURVE('',#3637,#3637,#3170,.T.);
#4327=EDGE_CURVE('',#3637,#3638,#2279,.T.);
#4328=EDGE_CURVE('',#3638,#3638,#3171,.T.);
#4329=EDGE_CURVE('',#3639,#3639,#3172,.T.);
#4330=EDGE_CURVE('',#3639,#3640,#2280,.T.);
#4331=EDGE_CURVE('',#3640,#3640,#3173,.T.);
#4332=EDGE_CURVE('',#3641,#3641,#3174,.T.);
#4333=EDGE_CURVE('',#3641,#3642,#2281,.T.);
#4334=EDGE_CURVE('',#3642,#3642,#3175,.T.);
#4335=EDGE_CURVE('',#3643,#3643,#3176,.T.);
#4336=EDGE_CURVE('',#3644,#3644,#3177,.T.);
#4337=EDGE_CURVE('',#3644,#3643,#2282,.T.);
#4338=EDGE_CURVE('',#3645,#3645,#3178,.T.);
#4339=EDGE_CURVE('',#3645,#3646,#2283,.T.);
#4340=EDGE_CURVE('',#3646,#3646,#3179,.T.);
#5388=ORIENTED_EDGE('',*,*,#4320,.F.);
#5389=ORIENTED_EDGE('',*,*,#4321,.T.);
#5390=ORIENTED_EDGE('',*,*,#4322,.F.);
#5391=ORIENTED_EDGE('',*,*,#4321,.F.);
#5392=ORIENTED_EDGE('',*,*,#4323,.F.);
#5393=ORIENTED_EDGE('',*,*,#4324,.T.);
#5394=ORIENTED_EDGE('',*,*,#4325,.F.);
#5395=ORIENTED_EDGE('',*,*,#4324,.F.);
#5396=ORIENTED_EDGE('',*,*,#4326,.F.);
#5397=ORIENTED_EDGE('',*,*,#4327,.T.);
#5398=ORIENTED_EDGE('',*,*,#4328,.F.);
#5399=ORIENTED_EDGE('',*,*,#4327,.F.);
#5400=ORIENTED_EDGE('',*,*,#4329,.F.);
#5401=ORIENTED_EDGE('',*,*,#4330,.T.);
#5402=ORIENTED_EDGE('',*,*,#4331,.F.);
#5403=ORIENTED_EDGE('',*,*,#4330,.F.);
#5404=ORIENTED_EDGE('',*,*,#4332,.F.);
#5405=ORIENTED_EDGE('',*,*,#4333,.T.);
#5406=ORIENTED_EDGE('',*,*,#4334,.T.);
#5407=ORIENTED_EDGE('',*,*,#4333,.F.);
#5408=ORIENTED_EDGE('',*,*,#4334,.F.);
#5409=ORIENTED_EDGE('',*,*,#4335,.F.);
#5410=ORIENTED_EDGE('',*,*,#4336,.F.);
#5411=ORIENTED_EDGE('',*,*,#4337,.T.);
#5412=ORIENTED_EDGE('',*,*,#4335,.T.);
#5413=ORIENTED_EDGE('',*,*,#4337,.F.);
#5414=ORIENTED_EDGE('',*,*,#4338,.F.);
#5415=ORIENTED_EDGE('',*,*,#4339,.T.);
#5416=ORIENTED_EDGE('',*,*,#4340,.T.);
#5417=ORIENTED_EDGE('',*,*,#4339,.F.);
#5418=ORIENTED_EDGE('',*,*,#4338,.T.);
#5419=ORIENTED_EDGE('',*,*,#4336,.T.);
#5420=ORIENTED_EDGE('',*,*,#4331,.T.);
#5421=ORIENTED_EDGE('',*,*,#4328,.T.);
#5422=ORIENTED_EDGE('',*,*,#4325,.T.);
#5423=ORIENTED_EDGE('',*,*,#4322,.T.);
#5424=ORIENTED_EDGE('',*,*,#4340,.F.);
#5425=ORIENTED_EDGE('',*,*,#4332,.T.);
#5426=ORIENTED_EDGE('',*,*,#4329,.T.);
#5427=ORIENTED_EDGE('',*,*,#4326,.T.);
#5428=ORIENTED_EDGE('',*,*,#4323,.T.);
#5429=ORIENTED_EDGE('',*,*,#4320,.T.);
#7073=CYLINDRICAL_SURFACE('',#8259,0.225);
#7074=CYLINDRICAL_SURFACE('',#8262,0.225);
#7075=CYLINDRICAL_SURFACE('',#8265,0.225);
#7076=CYLINDRICAL_SURFACE('',#8268,0.225);
#7077=CYLINDRICAL_SURFACE('',#8271,1.59);
#7078=CYLINDRICAL_SURFACE('',#8276,1.1);
#7079=CYLINDRICAL_SURFACE('',#8278,2.5);
#7259=ADVANCED_FACE('',(#1148),#7073,.F.);
#7260=ADVANCED_FACE('',(#1149),#7074,.F.);
#7261=ADVANCED_FACE('',(#1150),#7075,.F.);
#7262=ADVANCED_FACE('',(#1151),#7076,.F.);
#7263=ADVANCED_FACE('',(#1152),#7077,.T.);
#7264=ADVANCED_FACE('',(#1153,#695),#894,.F.);
#7265=ADVANCED_FACE('',(#1154),#7078,.F.);
#7266=ADVANCED_FACE('',(#1155),#7079,.T.);
#7267=ADVANCED_FACE('',(#1156,#696,#697,#698,#699,#700),#895,.T.);
#7268=ADVANCED_FACE('',(#1157,#701,#702,#703,#704,#705),#896,.F.);
#7658=CLOSED_SHELL('',(#7259,#7260,#7261,#7262,#7263,#7264,#7265,#7266,
#7267,#7268));
#8258=AXIS2_PLACEMENT_3D('',#11912,#9456,#9457);
#8259=AXIS2_PLACEMENT_3D('',#11913,#9458,#9459);
#8260=AXIS2_PLACEMENT_3D('',#11915,#9460,#9461);
#8261=AXIS2_PLACEMENT_3D('',#11918,#9463,#9464);
#8262=AXIS2_PLACEMENT_3D('',#11919,#9465,#9466);
#8263=AXIS2_PLACEMENT_3D('',#11921,#9467,#9468);
#8264=AXIS2_PLACEMENT_3D('',#11924,#9470,#9471);
#8265=AXIS2_PLACEMENT_3D('',#11925,#9472,#9473);
#8266=AXIS2_PLACEMENT_3D('',#11927,#9474,#9475);
#8267=AXIS2_PLACEMENT_3D('',#11930,#9477,#9478);
#8268=AXIS2_PLACEMENT_3D('',#11931,#9479,#9480);
#8269=AXIS2_PLACEMENT_3D('',#11933,#9481,#9482);
#8270=AXIS2_PLACEMENT_3D('',#11936,#9484,#9485);
#8271=AXIS2_PLACEMENT_3D('',#11937,#9486,#9487);
#8272=AXIS2_PLACEMENT_3D('',#11939,#9488,#9489);
#8273=AXIS2_PLACEMENT_3D('',#11942,#9491,#9492);
#8274=AXIS2_PLACEMENT_3D('',#11943,#9493,#9494);
#8275=AXIS2_PLACEMENT_3D('',#11945,#9495,#9496);
#8276=AXIS2_PLACEMENT_3D('',#11946,#9497,#9498);
#8277=AXIS2_PLACEMENT_3D('',#11948,#9499,#9500);
#8278=AXIS2_PLACEMENT_3D('',#11950,#9502,#9503);
#8279=AXIS2_PLACEMENT_3D('',#11952,#9504,#9505);
#8280=AXIS2_PLACEMENT_3D('',#11955,#9507,#9508);
#8281=AXIS2_PLACEMENT_3D('',#11956,#9509,#9510);
#8282=AXIS2_PLACEMENT_3D('',#11957,#9511,#9512);
#9456=DIRECTION('axis',(0.,0.,1.));
#9457=DIRECTION('refdir',(1.,0.,0.));
#9458=DIRECTION('center_axis',(0.,1.,0.));
#9459=DIRECTION('ref_axis',(1.,0.,0.));
#9460=DIRECTION('center_axis',(0.,1.,0.));
#9461=DIRECTION('ref_axis',(1.,0.,0.));
#9462=DIRECTION('',(0.,1.,0.));
#9463=DIRECTION('center_axis',(0.,-1.,0.));
#9464=DIRECTION('ref_axis',(1.,0.,0.));
#9465=DIRECTION('center_axis',(0.,1.,0.));
#9466=DIRECTION('ref_axis',(1.,0.,0.));
#9467=DIRECTION('center_axis',(0.,1.,0.));
#9468=DIRECTION('ref_axis',(1.,0.,0.));
#9469=DIRECTION('',(0.,1.,0.));
#9470=DIRECTION('center_axis',(0.,-1.,0.));
#9471=DIRECTION('ref_axis',(1.,0.,0.));
#9472=DIRECTION('center_axis',(0.,1.,0.));
#9473=DIRECTION('ref_axis',(1.,0.,0.));
#9474=DIRECTION('center_axis',(0.,1.,0.));
#9475=DIRECTION('ref_axis',(1.,0.,0.));
#9476=DIRECTION('',(0.,1.,0.));
#9477=DIRECTION('center_axis',(0.,-1.,0.));
#9478=DIRECTION('ref_axis',(1.,0.,0.));
#9479=DIRECTION('center_axis',(0.,1.,0.));
#9480=DIRECTION('ref_axis',(1.,0.,0.));
#9481=DIRECTION('center_axis',(0.,1.,0.));
#9482=DIRECTION('ref_axis',(1.,0.,0.));
#9483=DIRECTION('',(0.,1.,0.));
#9484=DIRECTION('center_axis',(0.,-1.,0.));
#9485=DIRECTION('ref_axis',(1.,0.,0.));
#9486=DIRECTION('center_axis',(0.,1.,0.));
#9487=DIRECTION('ref_axis',(1.,0.,0.));
#9488=DIRECTION('center_axis',(0.,1.,0.));
#9489=DIRECTION('ref_axis',(1.,0.,0.));
#9490=DIRECTION('',(0.,-1.,0.));
#9491=DIRECTION('center_axis',(0.,1.,0.));
#9492=DIRECTION('ref_axis',(1.,0.,0.));
#9493=DIRECTION('center_axis',(0.,1.,0.));
#9494=DIRECTION('ref_axis',(1.,0.,0.));
#9495=DIRECTION('center_axis',(0.,-1.,0.));
#9496=DIRECTION('ref_axis',(1.,0.,0.));
#9497=DIRECTION('center_axis',(0.,1.,0.));
#9498=DIRECTION('ref_axis',(1.,0.,0.));
#9499=DIRECTION('center_axis',(0.,-1.,0.));
#9500=DIRECTION('ref_axis',(1.,0.,0.));
#9501=DIRECTION('',(0.,-1.,0.));
#9502=DIRECTION('center_axis',(0.,1.,0.));
#9503=DIRECTION('ref_axis',(1.,0.,0.));
#9504=DIRECTION('center_axis',(0.,1.,0.));
#9505=DIRECTION('ref_axis',(1.,0.,0.));
#9506=DIRECTION('',(0.,-1.,0.));
#9507=DIRECTION('center_axis',(0.,1.,0.));
#9508=DIRECTION('ref_axis',(1.,0.,0.));
#9509=DIRECTION('center_axis',(0.,1.,0.));
#9510=DIRECTION('ref_axis',(1.,0.,0.));
#9511=DIRECTION('center_axis',(0.,1.,0.));
#9512=DIRECTION('ref_axis',(1.,0.,0.));
#11912=CARTESIAN_POINT('',(0.,0.,0.));
#11913=CARTESIAN_POINT('Origin',(-2.,-6.3,7.));
#11914=CARTESIAN_POINT('',(-2.225,-6.2,7.));
#11915=CARTESIAN_POINT('Origin',(-2.,-6.2,7.));
#11916=CARTESIAN_POINT('',(-2.225,-5.9,7.));
#11917=CARTESIAN_POINT('',(-2.225,-6.3,7.));
#11918=CARTESIAN_POINT('Origin',(-2.,-5.9,7.));
#11919=CARTESIAN_POINT('Origin',(1.22464679914735E-16,-6.3,9.));
#11920=CARTESIAN_POINT('',(-0.225,-6.2,9.));
#11921=CARTESIAN_POINT('Origin',(1.22464679914735E-16,-6.2,9.));
#11922=CARTESIAN_POINT('',(-0.225,-5.9,9.));
#11923=CARTESIAN_POINT('',(-0.225,-6.3,9.));
#11924=CARTESIAN_POINT('Origin',(1.22464679914735E-16,-5.9,9.));
#11925=CARTESIAN_POINT('Origin',(2.,-6.3,7.));
#11926=CARTESIAN_POINT('',(1.775,-6.2,7.));
#11927=CARTESIAN_POINT('Origin',(2.,-6.2,7.));
#11928=CARTESIAN_POINT('',(1.775,-5.9,7.));
#11929=CARTESIAN_POINT('',(1.775,-6.3,7.));
#11930=CARTESIAN_POINT('Origin',(2.,-5.9,7.));
#11931=CARTESIAN_POINT('Origin',(-3.67394039744206E-16,-6.3,5.));
#11932=CARTESIAN_POINT('',(-0.225,-6.2,5.));
#11933=CARTESIAN_POINT('Origin',(-3.67394039744206E-16,-6.2,5.));
#11934=CARTESIAN_POINT('',(-0.225,-5.9,5.));
#11935=CARTESIAN_POINT('',(-0.225,-6.3,5.));
#11936=CARTESIAN_POINT('Origin',(-3.67394039744206E-16,-5.9,5.));
#11937=CARTESIAN_POINT('Origin',(0.,-6.5,7.));
#11938=CARTESIAN_POINT('',(-1.59,-6.2,7.));
#11939=CARTESIAN_POINT('Origin',(0.,-6.2,7.));
#11940=CARTESIAN_POINT('',(-1.59,-6.5,7.));
#11941=CARTESIAN_POINT('',(-1.59,-6.5,7.));
#11942=CARTESIAN_POINT('Origin',(0.,-6.5,7.));
#11943=CARTESIAN_POINT('Origin',(0.,-6.5,7.));
#11944=CARTESIAN_POINT('',(-1.1,-6.5,7.));
#11945=CARTESIAN_POINT('Origin',(0.,-6.5,7.));
#11946=CARTESIAN_POINT('Origin',(0.,-6.2,7.));
#11947=CARTESIAN_POINT('',(-1.1,-5.9,7.));
#11948=CARTESIAN_POINT('Origin',(0.,-5.9,7.));
#11949=CARTESIAN_POINT('',(-1.1,-6.2,7.));
#11950=CARTESIAN_POINT('Origin',(0.,-6.2,7.));
#11951=CARTESIAN_POINT('',(-2.5,-5.9,7.));
#11952=CARTESIAN_POINT('Origin',(0.,-5.9,7.));
#11953=CARTESIAN_POINT('',(-2.5,-6.2,7.));
#11954=CARTESIAN_POINT('',(-2.5,-6.2,7.));
#11955=CARTESIAN_POINT('Origin',(0.,-6.2,7.));
#11956=CARTESIAN_POINT('Origin',(0.,-5.9,7.));
#11957=CARTESIAN_POINT('Origin',(0.,-6.2,7.));
#14738=UNCERTAINTY_MEASURE_WITH_UNIT(LENGTH_MEASURE(0.001),#14823,
'DISTANCE_ACCURACY_VALUE',
'Maximum model space distance between geometric entities at asserted c
onnectivities');
#14777=UNCERTAINTY_MEASURE_WITH_UNIT(LENGTH_MEASURE(0.001),#14823,
'DISTANCE_ACCURACY_VALUE',
'Maximum model space distance between geometric entities at asserted c
onnectivities');
#14783=(
GEOMETRIC_REPRESENTATION_CONTEXT(3)
GLOBAL_UNCERTAINTY_ASSIGNED_CONTEXT((#14738))
GLOBAL_UNIT_ASSIGNED_CONTEXT((#14823,#14825,#14826))
REPRESENTATION_CONTEXT('','3D')
);
#14822=(
GEOMETRIC_REPRESENTATION_CONTEXT(3)
GLOBAL_UNCERTAINTY_ASSIGNED_CONTEXT((#14777))
GLOBAL_UNIT_ASSIGNED_CONTEXT((#14823,#14825,#14826))
REPRESENTATION_CONTEXT('','3D')
);
#14823=(
LENGTH_UNIT()
NAMED_UNIT(*)
SI_UNIT(.CENTI.,.METRE.)
);
#14825=(
NAMED_UNIT(*)
PLANE_ANGLE_UNIT()
SI_UNIT($,.RADIAN.)
);
#14826=(
NAMED_UNIT(*)
SI_UNIT($,.STERADIAN.)
SOLID_ANGLE_UNIT()
);
#14832=SHAPE_DEFINITION_REPRESENTATION(#14876,#15003);
#14876=PRODUCT_DEFINITION_SHAPE('',$,#15048);
#15003=SHAPE_REPRESENTATION('',(#8258),#14783);
#15042=PRODUCT_DEFINITION_CONTEXT('part definition',#15176,'design');
#15048=PRODUCT_DEFINITION('Support cap (1)','Support cap (1)',#15092,#15042);
#15092=PRODUCT_DEFINITION_FORMATION('',$,#15183);
#15176=APPLICATION_CONTEXT(
'Core Data for Automotive Mechanical Design Process');
#15177=PRODUCT_CONTEXT('part definition',#15176,'mechanical');
#15183=PRODUCT('Support cap (1)','Support cap (1)','Support cap (1)',(#15177));
#15271=COLOUR_RGB('Sky Blue',0.24,0.69,0.87);
#15272=FILL_AREA_STYLE_COLOUR('',#15271);
#15273=FILL_AREA_STYLE('',(#15272));
#15274=SURFACE_STYLE_FILL_AREA(#15273);
#15275=SURFACE_SIDE_STYLE('',(#15274));
#15276=SURFACE_STYLE_USAGE(.BOTH.,#15275);
#15277=PRESENTATION_STYLE_ASSIGNMENT((#15276));
ENDSEC;
END-ISO-10303-21;
